ISO-10303-21;
HEADER;
FILE_DESCRIPTION (('STEP AP214'),
    '1' );
FILE_NAME ('Pivot Pins.step',
    '2026-10-06T14:27:08',
    ( '' ),
    ( '' ),
    'SwSTEP 2.0',
    'SolidWorks 2020',
    '' );
FILE_SCHEMA (( 'AUTOMOTIVE_DESIGN' ));
ENDSEC;

DATA;
#179=AXIS2_PLACEMENT_3D ( 'NONE', #33313, #30308, #33738 ) ;
#194=DIRECTION ( 'NONE',  ( 1.000000000000000000, 0.000000000000000000, 0.000000000000000000 ) ) ;
#272=CARTESIAN_POINT ( 'NONE',  ( -14.60500000000000220, 71.11999999999999034, -5.080000000000000959 ) ) ;
#599=DIRECTION ( 'NONE',  ( 1.000000000000000000, 0.000000000000000000, -3.035386659626960118E-16 ) ) ;
#804=PLANE ( 'NONE',  #34407 ) ;
#838=ADVANCED_FACE ( 'NONE', ( #21965 ), #39369, .T. ) ;
#1080=EDGE_LOOP ( 'NONE', ( #11911, #34503, #25339, #40906 ) ) ;
#1225=ORIENTED_EDGE ( 'NONE', *, *, #17010, .F. ) ;
#1696=ADVANCED_FACE ( 'NONE', ( #11137 ), #26704, .T. ) ;
#1824=VERTEX_POINT ( 'NONE', #11551 ) ;
#1870=CIRCLE ( 'NONE', #37222, 1.905000000000007354 ) ;
#2283=ADVANCED_FACE ( 'NONE', ( #16420 ), #6435, .T. ) ;
#2508=SURFACE_STYLE_USAGE ( .BOTH. , #31667 ) ;
#2622=DIRECTION ( 'NONE',  ( 0.000000000000000000, 0.000000000000000000, -1.000000000000000000 ) ) ;
#2672=CLOSED_SHELL ( 'NONE', ( #32343, #838, #24751, #2283, #1696, #39917, #26378, #30390 ) ) ;
#2773=CONICAL_SURFACE ( 'NONE', #27236, 2.540000000000002256, 0.7853981633974523868 ) ;
#2902=DIRECTION ( 'NONE',  ( 3.035386659626960118E-16, -0.000000000000000000, 1.000000000000000000 ) ) ;
#3275=AXIS2_PLACEMENT_3D ( 'NONE', #6670, #19223, #39468 ) ;
#3341=DIRECTION ( 'NONE',  ( -1.000000000000000000, 0.000000000000000000, 4.553079989440437711E-16 ) ) ;
#3469=ORIENTED_EDGE ( 'NONE', *, *, #5401, .T. ) ;
#3670=DIRECTION ( 'NONE',  ( -3.035386659626960118E-16, 0.000000000000000000, -1.000000000000000000 ) ) ;
#4119=SURFACE_STYLE_USAGE ( .BOTH. , #33289 ) ;
#4534=PRODUCT ( 'Pivot Pins', 'Pivot Pins', '', ( #27049 ) ) ;
#4649=DIRECTION ( 'NONE',  ( -0.000000000000000000, -0.000000000000000000, 1.000000000000000000 ) ) ;
#4650=STYLED_ITEM ( 'NONE', ( #13892 ), #38189 ) ;
#4686=DIRECTION ( 'NONE',  ( 0.000000000000000000, 0.000000000000000000, -1.000000000000000000 ) ) ;
#4832=ORIENTED_EDGE ( 'NONE', *, *, #30047, .F. ) ;
#4986=CARTESIAN_POINT ( 'NONE',  ( -15.23999999999999311, 71.11999999999999034, 5.714999999999998970 ) ) ;
#4994=AXIS2_PLACEMENT_3D ( 'NONE', #22748, #9988, #19993 ) ;
#5367=AXIS2_PLACEMENT_3D ( 'NONE', #29426, #3670, #38606 ) ;
#5401=EDGE_CURVE ( 'NONE', #1824, #8452, #9771, .T. ) ;
#5566=EDGE_CURVE ( 'NONE', #26975, #29909, #36507, .T. ) ;
#5583=( NAMED_UNIT ( * ) SI_UNIT ( $, .STERADIAN. ) SOLID_ANGLE_UNIT ( ) );
#5595=VERTEX_POINT ( 'NONE', #7126 ) ;
#5606=AXIS2_PLACEMENT_3D ( 'NONE', #11506, #30065, #7285 ) ;
#5698=DIRECTION ( 'NONE',  ( 3.035386659626960118E-16, -0.000000000000000000, 1.000000000000000000 ) ) ;
#5703=SURFACE_STYLE_FILL_AREA ( #18661 ) ;
#5894=DIRECTION ( 'NONE',  ( -3.035386659626960118E-16, 0.000000000000000000, -1.000000000000000000 ) ) ;
#5911=CARTESIAN_POINT ( 'NONE',  ( -17.14500000000000313, 71.11999999999999034, -5.714999999999998970 ) ) ;
#6276=ORIENTED_EDGE ( 'NONE', *, *, #37635, .T. ) ;
#6435=PLANE ( 'NONE',  #5367 ) ;
#6621=( GEOMETRIC_REPRESENTATION_CONTEXT ( 3 ) GLOBAL_UNCERTAINTY_ASSIGNED_CONTEXT ( ( #39338 ) ) GLOBAL_UNIT_ASSIGNED_CONTEXT ( ( #25692, #25899, #6740 ) ) REPRESENTATION_CONTEXT ( 'NONE', 'WORKASPACE' ) );
#6670=CARTESIAN_POINT ( 'NONE',  ( 0.000000000000000000, 0.000000000000000000, 0.000000000000000000 ) ) ;
#6740=( NAMED_UNIT ( * ) SI_UNIT ( $, .STERADIAN. ) SOLID_ANGLE_UNIT ( ) );
#7126=CARTESIAN_POINT ( 'NONE',  ( -14.60499999999999865, 71.11999999999999034, 5.079999999999997407 ) ) ;
#7166=CARTESIAN_POINT ( 'NONE',  ( -19.68500000000000227, 71.11999999999999034, 5.079999999999997407 ) ) ;
#7172=CARTESIAN_POINT ( 'NONE',  ( -19.68500000000000938, 71.11999999999999034, -5.080000000000000959 ) ) ;
#7285=DIRECTION ( 'NONE',  ( -1.000000000000000000, 0.000000000000000000, 0.000000000000000000 ) ) ;
#7384=ORIENTED_EDGE ( 'NONE', *, *, #8269, .T. ) ;
#7522=VECTOR ( 'NONE', #20859, 1000.000000000000000 ) ;
#7779=VECTOR ( 'NONE', #20286, 1000.000000000000114 ) ;
#7871=FACE_OUTER_BOUND ( 'NONE', #20094, .T. ) ;
#8089=EDGE_CURVE ( 'NONE', #29909, #11064, #9752, .T. ) ;
#8269=EDGE_CURVE ( 'NONE', #29132, #1824, #8415, .T. ) ;
#8322=DIRECTION ( 'NONE',  ( 1.000000000000000000, 0.000000000000000000, 0.000000000000000000 ) ) ;
#8415=CIRCLE ( 'NONE', #33577, 1.905000000000007354 ) ;
#8452=VERTEX_POINT ( 'NONE', #7166 ) ;
#8507=ORIENTED_EDGE ( 'NONE', *, *, #40447, .F. ) ;
#9075=DIRECTION ( 'NONE',  ( 1.000000000000000000, 0.000000000000000000, -4.553079989440420948E-16 ) ) ;
#9613=CARTESIAN_POINT ( 'NONE',  ( -17.14499999999999957, 71.11999999999999034, 5.714999999999999858 ) ) ;
#9752=CIRCLE ( 'NONE', #30847, 2.540000000000004032 ) ;
#9754=EDGE_CURVE ( 'NONE', #5595, #8452, #12918, .T. ) ;
#9771=LINE ( 'NONE', #35766, #19300 ) ;
#9988=DIRECTION ( 'NONE',  ( 3.035386659626960118E-16, -0.000000000000000000, 1.000000000000000000 ) ) ;
#10359=UNCERTAINTY_MEASURE_WITH_UNIT (LENGTH_MEASURE( 1.000000000000000082E-05 ), #40102, 'distance_accuracy_value', 'NONE');
#10485=SURFACE_STYLE_FILL_AREA ( #30494 ) ;
#10551=ORIENTED_EDGE ( 'NONE', *, *, #9754, .T. ) ;
#10686=ORIENTED_EDGE ( 'NONE', *, *, #8089, .T. ) ;
#10690=( LENGTH_UNIT ( ) NAMED_UNIT ( * ) SI_UNIT ( .MILLI., .METRE. ) );
#10787=MANIFOLD_SOLID_BREP ( 'Stock-MAS-162-1', #2672 ) ;
#10866=EDGE_CURVE ( 'NONE', #26975, #41779, #14084, .T. ) ;
#11064=VERTEX_POINT ( 'NONE', #7172 ) ;
#11137=FACE_OUTER_BOUND ( 'NONE', #17088, .T. ) ;
#11427=DIRECTION ( 'NONE',  ( -1.000000000000000000, 0.000000000000000000, 0.000000000000000000 ) ) ;
#11506=CARTESIAN_POINT ( 'NONE',  ( -17.14500000000000313, 71.11999999999999034, -5.080000000000000959 ) ) ;
#11524=SHAPE_REPRESENTATION_RELATIONSHIP ( 'NONE' , 'NONE' ,  #26424, #38189 ) ;
#11551=CARTESIAN_POINT ( 'NONE',  ( -19.05000000000000782, 71.11999999999999034, 5.715000000000000746 ) ) ;
#11625=CARTESIAN_POINT ( 'NONE',  ( -17.14500000000000313, 71.11999999999999034, -5.714999999999998970 ) ) ;
#11632=AXIS2_PLACEMENT_3D ( 'NONE', #17230, #4686, #24038 ) ;
#11911=ORIENTED_EDGE ( 'NONE', *, *, #8269, .F. ) ;
#11994=VECTOR ( 'NONE', #16162, 1000.000000000000114 ) ;
#12564=FACE_OUTER_BOUND ( 'NONE', #33881, .T. ) ;
#12656=EDGE_LOOP ( 'NONE', ( #24279, #36913 ) ) ;
#12842=AXIS2_PLACEMENT_3D ( 'NONE', #9613, #2622, #41809 ) ;
#12918=CIRCLE ( 'NONE', #23797, 2.540000000000002256 ) ;
#13252=ORIENTED_EDGE ( 'NONE', *, *, #22183, .F. ) ;
#13765=PRODUCT_DEFINITION_CONTEXT ( 'detailed design', #33067, 'design' ) ;
#13892=PRESENTATION_STYLE_ASSIGNMENT (( #4119 ) ) ;
#14084=CIRCLE ( 'NONE', #28381, 1.905000000000000471 ) ;
#14452=CONICAL_SURFACE ( 'NONE', #29417, 2.540000000000002256, 0.7853981633974523868 ) ;
#14676=DIRECTION ( 'NONE',  ( -0.000000000000000000, 0.000000000000000000, -1.000000000000000000 ) ) ;
#14923=( NAMED_UNIT ( * ) PLANE_ANGLE_UNIT ( ) SI_UNIT ( $, .RADIAN. ) );
#15501=FACE_OUTER_BOUND ( 'NONE', #27340, .T. ) ;
#15657=CARTESIAN_POINT ( 'NONE',  ( -15.24000000000000554, 71.11999999999999034, -5.714999999999999858 ) ) ;
#15706=VECTOR ( 'NONE', #19188, 1000.000000000000000 ) ;
#16162=DIRECTION ( 'NONE',  ( -0.7071067811865504593, 8.659560562354968603E-17, 0.7071067811865445751 ) ) ;
#16420=FACE_OUTER_BOUND ( 'NONE', #12656, .T. ) ;
#16796=ORIENTED_EDGE ( 'NONE', *, *, #10866, .F. ) ;
#16808=CARTESIAN_POINT ( 'NONE',  ( -19.68500000000000227, 71.11999999999999034, 5.714999999999998970 ) ) ;
#17010=EDGE_CURVE ( 'NONE', #29909, #5595, #18084, .T. ) ;
#17088=EDGE_LOOP ( 'NONE', ( #13252, #34853, #22935, #10551 ) ) ;
#17230=CARTESIAN_POINT ( 'NONE',  ( -17.14499999999999957, 71.11999999999999034, 5.714999999999999858 ) ) ;
#17635=ORIENTED_EDGE ( 'NONE', *, *, #40447, .T. ) ;
#17699=( NAMED_UNIT ( * ) PLANE_ANGLE_UNIT ( ) SI_UNIT ( $, .RADIAN. ) );
#18066=EDGE_CURVE ( 'NONE', #29132, #5595, #22574, .T. ) ;
#18084=LINE ( 'NONE', #40490, #7522 ) ;
#18228=( GEOMETRIC_REPRESENTATION_CONTEXT ( 3 ) GLOBAL_UNCERTAINTY_ASSIGNED_CONTEXT ( ( #29540 ) ) GLOBAL_UNIT_ASSIGNED_CONTEXT ( ( #10690, #14923, #5583 ) ) REPRESENTATION_CONTEXT ( 'NONE', 'WORKASPACE' ) );
#18281=ORIENTED_EDGE ( 'NONE', *, *, #9754, .F. ) ;
#18294=EDGE_CURVE ( 'NONE', #8452, #5595, #41586, .T. ) ;
#18661=FILL_AREA_STYLE ('',( #41264 ) ) ;
#18855=DIRECTION ( 'NONE',  ( -1.000000000000000000, 0.000000000000000000, 4.553079989440437711E-16 ) ) ;
#18872=DIRECTION ( 'NONE',  ( -3.035386659626960118E-16, 0.000000000000000000, -1.000000000000000000 ) ) ;
#18925=PRODUCT_DEFINITION_FORMATION_WITH_SPECIFIED_SOURCE ( 'ANY', '', #4534, .NOT_KNOWN. ) ;
#19101=EDGE_LOOP ( 'NONE', ( #10686, #36520, #26672, #1225 ) ) ;
#19128=DIRECTION ( 'NONE',  ( -0.000000000000000000, 0.000000000000000000, -1.000000000000000000 ) ) ;
#19188=DIRECTION ( 'NONE',  ( 0.7071067811865436870, 8.659560562354886020E-17, -0.7071067811865513475 ) ) ;
#19223=DIRECTION ( 'NONE',  ( 0.000000000000000000, 0.000000000000000000, 1.000000000000000000 ) ) ;
#19300=VECTOR ( 'NONE', #19346, 1000.000000000000000 ) ;
#19346=DIRECTION ( 'NONE',  ( -0.7071067811865436870, 0.000000000000000000, -0.7071067811865513475 ) ) ;
#19993=DIRECTION ( 'NONE',  ( 1.000000000000000000, 0.000000000000000000, -3.414809992080326065E-16 ) ) ;
#19997=LINE ( 'NONE', #16808, #24434 ) ;
#20094=EDGE_LOOP ( 'NONE', ( #28306, #8507, #3469, #18281 ) ) ;
#20262=FILL_AREA_STYLE_COLOUR ( '', #33221 ) ;
#20286=DIRECTION ( 'NONE',  ( 0.7071067811865504593, 0.000000000000000000, 0.7071067811865445751 ) ) ;
#20859=DIRECTION ( 'NONE',  ( 3.035386659626960118E-16, -0.000000000000000000, 1.000000000000000000 ) ) ;
#20881=PRODUCT_DEFINITION ( 'UNKNOWN', '', #18925, #13765 ) ;
#21041=DIRECTION ( 'NONE',  ( 3.035386659626960118E-16, -0.000000000000000000, 1.000000000000000000 ) ) ;
#21249=DIRECTION ( 'NONE',  ( 0.000000000000000000, -0.000000000000000000, 1.000000000000000000 ) ) ;
#21877=CARTESIAN_POINT ( 'NONE',  ( -17.14500000000000313, 71.11999999999999034, -5.080000000000000959 ) ) ;
#21965=FACE_OUTER_BOUND ( 'NONE', #1080, .T. ) ;
#22094=ORIENTED_EDGE ( 'NONE', *, *, #26696, .F. ) ;
#22183=EDGE_CURVE ( 'NONE', #11064, #8452, #19997, .T. ) ;
#22196=CARTESIAN_POINT ( 'NONE',  ( -19.05000000000000426, 71.11999999999999034, -5.714999999999998082 ) ) ;
#22212=COLOUR_RGB ( '', 0.66274510, 0.83137255, 0.94901961) ;
#22474=AXIS2_PLACEMENT_3D ( 'NONE', #26852, #14676, #39859 ) ;
#22574=LINE ( 'NONE', #29195, #15706 ) ;
#22748=CARTESIAN_POINT ( 'NONE',  ( -17.14499999999999957, 71.11999999999999034, 5.714999999999998082 ) ) ;
#22935=ORIENTED_EDGE ( 'NONE', *, *, #17010, .T. ) ;
#23155=AXIS2_PLACEMENT_3D ( 'NONE', #11625, #5894, #18855 ) ;
#23797=AXIS2_PLACEMENT_3D ( 'NONE', #30876, #19128, #194 ) ;
#23836=SHAPE_DEFINITION_REPRESENTATION ( #40242, #26424 ) ;
#24038=DIRECTION ( 'NONE',  ( -1.000000000000000000, 0.000000000000000000, 0.000000000000000000 ) ) ;
#24210=PRESENTATION_STYLE_ASSIGNMENT (( #2508 ) ) ;
#24279=ORIENTED_EDGE ( 'NONE', *, *, #10866, .T. ) ;
#24305=( NAMED_UNIT ( * ) SI_UNIT ( $, .STERADIAN. ) SOLID_ANGLE_UNIT ( ) );
#24434=VECTOR ( 'NONE', #21041, 1000.000000000000000 ) ;
#24751=ADVANCED_FACE ( 'NONE', ( #35779 ), #31308, .T. ) ;
#25224=CIRCLE ( 'NONE', #23155, 1.905000000000000471 ) ;
#25339=ORIENTED_EDGE ( 'NONE', *, *, #18294, .F. ) ;
#25414=CONICAL_SURFACE ( 'NONE', #11632, 1.905000000000007354, 0.7853981633974428389 ) ;
#25486=CARTESIAN_POINT ( 'NONE',  ( -17.14499999999999957, 71.11999999999999034, 5.714999999999999858 ) ) ;
#25692=( LENGTH_UNIT ( ) NAMED_UNIT ( * ) SI_UNIT ( .MILLI., .METRE. ) );
#25899=( NAMED_UNIT ( * ) PLANE_ANGLE_UNIT ( ) SI_UNIT ( $, .RADIAN. ) );
#26378=ADVANCED_FACE ( 'NONE', ( #7871 ), #25414, .T. ) ;
#26424=SHAPE_REPRESENTATION ( 'Pivot Pins', ( #3275 ), #32513 ) ;
#26672=ORIENTED_EDGE ( 'NONE', *, *, #18294, .T. ) ;
#26685=EDGE_LOOP ( 'NONE', ( #17635, #7384 ) ) ;
#26696=EDGE_CURVE ( 'NONE', #41779, #26975, #25224, .T. ) ;
#26704=CYLINDRICAL_SURFACE ( 'NONE', #179, 2.540000000000002256 ) ;
#26852=CARTESIAN_POINT ( 'NONE',  ( -17.14499999999999957, 71.11999999999999034, 5.079999999999997407 ) ) ;
#26975=VERTEX_POINT ( 'NONE', #15657 ) ;
#27049=PRODUCT_CONTEXT ( 'NONE', #28694, 'mechanical' ) ;
#27236=AXIS2_PLACEMENT_3D ( 'NONE', #21877, #21249, #38306 ) ;
#27340=EDGE_LOOP ( 'NONE', ( #22094, #6276, #40561, #41316 ) ) ;
#27760=MECHANICAL_DESIGN_GEOMETRIC_PRESENTATION_REPRESENTATION('',(#4650),#18228);
#28117=DIRECTION ( 'NONE',  ( 0.000000000000000000, -0.000000000000000000, 1.000000000000000000 ) ) ;
#28306=ORIENTED_EDGE ( 'NONE', *, *, #18066, .F. ) ;
#28381=AXIS2_PLACEMENT_3D ( 'NONE', #5911, #18872, #3341 ) ;
#28694=APPLICATION_CONTEXT ( 'automotive_design' ) ;
#29132=VERTEX_POINT ( 'NONE', #4986 ) ;
#29195=CARTESIAN_POINT ( 'NONE',  ( -15.23999999999999311, 71.11999999999999034, 5.714999999999999858 ) ) ;
#29384=LINE ( 'NONE', #38979, #11994 ) ;
#29417=AXIS2_PLACEMENT_3D ( 'NONE', #37497, #28117, #8322 ) ;
#29426=CARTESIAN_POINT ( 'NONE',  ( -17.14500000000000313, 71.11999999999999034, -5.714999999999998970 ) ) ;
#29540=UNCERTAINTY_MEASURE_WITH_UNIT (LENGTH_MEASURE( 1.000000000000000082E-05 ), #10690, 'distance_accuracy_value', 'NONE');
#29909=VERTEX_POINT ( 'NONE', #272 ) ;
#30047=EDGE_CURVE ( 'NONE', #11064, #29909, #33511, .T. ) ;
#30065=DIRECTION ( 'NONE',  ( -0.000000000000000000, -0.000000000000000000, 1.000000000000000000 ) ) ;
#30176=CARTESIAN_POINT ( 'NONE',  ( -14.60499999999999865, 71.11999999999999034, 5.714999999999998970 ) ) ;
#30308=DIRECTION ( 'NONE',  ( 3.035386659626960118E-16, -0.000000000000000000, 1.000000000000000000 ) ) ;
#30390=ADVANCED_FACE ( 'NONE', ( #12564 ), #14452, .T. ) ;
#30494=FILL_AREA_STYLE ('',( #20262 ) ) ;
#30847=AXIS2_PLACEMENT_3D ( 'NONE', #34238, #4649, #11427 ) ;
#30876=CARTESIAN_POINT ( 'NONE',  ( -17.14499999999999957, 71.11999999999999034, 5.079999999999997407 ) ) ;
#31084=MECHANICAL_DESIGN_GEOMETRIC_PRESENTATION_REPRESENTATION('',(#41382),#6621);
#31308=CYLINDRICAL_SURFACE ( 'NONE', #4994, 2.540000000000002256 ) ;
#31667=SURFACE_SIDE_STYLE ('',( #5703 ) ) ;
#32343=ADVANCED_FACE ( 'NONE', ( #15501 ), #2773, .T. ) ;
#32513=( GEOMETRIC_REPRESENTATION_CONTEXT ( 3 ) GLOBAL_UNCERTAINTY_ASSIGNED_CONTEXT ( ( #10359 ) ) GLOBAL_UNIT_ASSIGNED_CONTEXT ( ( #40102, #17699, #24305 ) ) REPRESENTATION_CONTEXT ( 'NONE', 'WORKASPACE' ) );
#33067=APPLICATION_CONTEXT ( 'automotive_design' ) ;
#33221=COLOUR_RGB ( '', 0.66274510, 0.83137255, 0.94901961) ;
#33289=SURFACE_SIDE_STYLE ('',( #10485 ) ) ;
#33313=CARTESIAN_POINT ( 'NONE',  ( -17.14499999999999957, 71.11999999999999034, 5.714999999999998082 ) ) ;
#33511=CIRCLE ( 'NONE', #5606, 2.540000000000004032 ) ;
#33577=AXIS2_PLACEMENT_3D ( 'NONE', #25486, #5698, #35712 ) ;
#33738=DIRECTION ( 'NONE',  ( 1.000000000000000000, 0.000000000000000000, -3.414809992080326065E-16 ) ) ;
#33881=EDGE_LOOP ( 'NONE', ( #37117, #16796, #38963, #4832 ) ) ;
#34238=CARTESIAN_POINT ( 'NONE',  ( -17.14500000000000313, 71.11999999999999034, -5.080000000000000959 ) ) ;
#34407=AXIS2_PLACEMENT_3D ( 'NONE', #30176, #39786, #599 ) ;
#34503=ORIENTED_EDGE ( 'NONE', *, *, #18066, .T. ) ;
#34853=ORIENTED_EDGE ( 'NONE', *, *, #30047, .T. ) ;
#35712=DIRECTION ( 'NONE',  ( 1.000000000000000000, 0.000000000000000000, -4.553079989440420948E-16 ) ) ;
#35766=CARTESIAN_POINT ( 'NONE',  ( -19.05000000000000782, 71.11999999999999034, 5.714999999999999858 ) ) ;
#35779=FACE_OUTER_BOUND ( 'NONE', #19101, .T. ) ;
#36507=LINE ( 'NONE', #39922, #7779 ) ;
#36520=ORIENTED_EDGE ( 'NONE', *, *, #22183, .T. ) ;
#36913=ORIENTED_EDGE ( 'NONE', *, *, #26696, .T. ) ;
#37117=ORIENTED_EDGE ( 'NONE', *, *, #37635, .F. ) ;
#37222=AXIS2_PLACEMENT_3D ( 'NONE', #41669, #2902, #9075 ) ;
#37497=CARTESIAN_POINT ( 'NONE',  ( -17.14500000000000313, 71.11999999999999034, -5.080000000000000959 ) ) ;
#37635=EDGE_CURVE ( 'NONE', #41779, #11064, #29384, .T. ) ;
#38189=ADVANCED_BREP_SHAPE_REPRESENTATION ( '', ( #10787, #3275 ), #32513 ) ;
#38306=DIRECTION ( 'NONE',  ( 1.000000000000000000, 0.000000000000000000, 0.000000000000000000 ) ) ;
#38606=DIRECTION ( 'NONE',  ( -1.000000000000000000, 0.000000000000000000, 3.035386659626960118E-16 ) ) ;
#38963=ORIENTED_EDGE ( 'NONE', *, *, #5566, .T. ) ;
#38979=CARTESIAN_POINT ( 'NONE',  ( -19.68500000000000938, 71.11999999999999034, -5.080000000000000959 ) ) ;
#39338=UNCERTAINTY_MEASURE_WITH_UNIT (LENGTH_MEASURE( 1.000000000000000082E-05 ), #25692, 'distance_accuracy_value', 'NONE');
#39369=CONICAL_SURFACE ( 'NONE', #12842, 1.905000000000007354, 0.7853981633974428389 ) ;
#39468=DIRECTION ( 'NONE',  ( 1.000000000000000000, 0.000000000000000000, 0.000000000000000000 ) ) ;
#39786=DIRECTION ( 'NONE',  ( 3.035386659626960118E-16, -0.000000000000000000, 1.000000000000000000 ) ) ;
#39859=DIRECTION ( 'NONE',  ( 1.000000000000000000, 0.000000000000000000, 0.000000000000000000 ) ) ;
#39917=ADVANCED_FACE ( 'NONE', ( #39996 ), #804, .T. ) ;
#39922=CARTESIAN_POINT ( 'NONE',  ( -14.60500000000000220, 71.11999999999999034, -5.080000000000000959 ) ) ;
#39996=FACE_OUTER_BOUND ( 'NONE', #26685, .T. ) ;
#40102=( LENGTH_UNIT ( ) NAMED_UNIT ( * ) SI_UNIT ( .MILLI., .METRE. ) );
#40242=PRODUCT_DEFINITION_SHAPE ( 'NONE', 'NONE',  #20881 ) ;
#40447=EDGE_CURVE ( 'NONE', #1824, #29132, #1870, .T. ) ;
#40490=CARTESIAN_POINT ( 'NONE',  ( -14.60499999999999865, 71.11999999999999034, 5.714999999999997193 ) ) ;
#40561=ORIENTED_EDGE ( 'NONE', *, *, #8089, .F. ) ;
#40906=ORIENTED_EDGE ( 'NONE', *, *, #5401, .F. ) ;
#41264=FILL_AREA_STYLE_COLOUR ( '', #22212 ) ;
#41316=ORIENTED_EDGE ( 'NONE', *, *, #5566, .F. ) ;
#41382=STYLED_ITEM ( 'NONE', ( #24210 ), #10787 ) ;
#41586=CIRCLE ( 'NONE', #22474, 2.540000000000002256 ) ;
#41669=CARTESIAN_POINT ( 'NONE',  ( -17.14499999999999957, 71.11999999999999034, 5.714999999999999858 ) ) ;
#41779=VERTEX_POINT ( 'NONE', #22196 ) ;
#41809=DIRECTION ( 'NONE',  ( -1.000000000000000000, 0.000000000000000000, 0.000000000000000000 ) ) ;
ENDSEC;
END-ISO-10303-21;
